ISO-10303-21;
HEADER;
FILE_DESCRIPTION (('STEP AP214'),
    '1' );
FILE_NAME ('socket head cap screw_am_B18.3.1M - 10 x 1.5 x 130 Hex SHCS -- 32NHX.step',
    '2026-10-24T15:53:57',
    ( '' ),
    ( '' ),
    'SwSTEP 2.0',
    'SolidWorks 2025',
    '' );
FILE_SCHEMA (( 'AUTOMOTIVE_DESIGN' ));
ENDSEC;

DATA;
#18=VERTEX_POINT ( 'NONE', #2644 ) ;
#32=CARTESIAN_POINT ( 'NONE',  ( 1.000000000000000888, 0.000000000000000000, 0.000000000000000000 ) ) ;
#35=ORIENTED_EDGE ( 'NONE', *, *, #4431, .T. ) ;
#46=EDGE_LOOP ( 'NONE', ( #354, #6549, #4798, #4239, #7292 ) ) ;
#69=EDGE_CURVE ( 'NONE', #4173, #3196, #7937, .T. ) ;
#73=ORIENTED_EDGE ( 'NONE', *, *, #8357, .F. ) ;
#78=ORIENTED_EDGE ( 'NONE', *, *, #1161, .F. ) ;
#79=VERTEX_POINT ( 'NONE', #7978 ) ;
#83=SHAPE_REPRESENTATION ( 'socket head cap screw_am_B18.3.1M - 10 x 1.5 x 130 Hex SHCS -- 32NHX', ( #7563 ), #2282 ) ;
#88=VECTOR ( 'NONE', #1875, 1000.000000000000000 ) ;
#120=APPLICATION_CONTEXT ( 'automotive_design' ) ;
#131=AXIS2_PLACEMENT_3D ( 'NONE', #4497, #4378, #2324 ) ;
#137=VECTOR ( 'NONE', #6845, 1000.000000000000000 ) ;
#146=ORIENTED_EDGE ( 'NONE', *, *, #4273, .F. ) ;
#148=CARTESIAN_POINT ( 'NONE',  ( 5.000000000000004441, 2.342598717236861638, 4.057500000000047180 ) ) ;
#196=ORIENTED_EDGE ( 'NONE', *, *, #805, .T. ) ;
#203=CARTESIAN_POINT ( 'NONE',  ( 5.000000000000115463, 7.027796151710889561, -4.057500000000047180 ) ) ;
#207=EDGE_LOOP ( 'NONE', ( #1622, #7247, #78 ) ) ;
#208=EDGE_CURVE ( 'NONE', #8055, #316, #7571, .T. ) ;
#209=CARTESIAN_POINT ( 'NONE',  ( 10.00000000000000888, 8.000000000000001776, 4.440892098500626162E-13 ) ) ;
#213=CYLINDRICAL_SURFACE ( 'NONE', #3938, 5.000000000000034639 ) ;
#220=DIRECTION ( 'NONE',  ( -1.774937036747276562E-30, -1.000000000000000000, -5.322451846059955323E-30 ) ) ;
#222=EDGE_CURVE ( 'NONE', #7027, #6175, #4345, .T. ) ;
#224=ORIENTED_EDGE ( 'NONE', *, *, #6569, .F. ) ;
#225=CARTESIAN_POINT ( 'NONE',  ( 5.000000000000115463, 7.027796151710889561, -4.057500000000047180 ) ) ;
#254=EDGE_CURVE ( 'NONE', #4707, #18, #5614, .T. ) ;
#260=CARTESIAN_POINT ( 'NONE',  ( 0.000000000000000000, -2.342598717236902939, 4.057500000000047180 ) ) ;
#266=CONICAL_SURFACE ( 'NONE', #4861, 4.171999999999999709, 0.7853981633975604115 ) ;
#277=ADVANCED_FACE ( 'NONE', ( #3520 ), #6195, .F. ) ;
#282=VERTEX_POINT ( 'NONE', #3737 ) ;
#291=DIRECTION ( 'NONE',  ( 0.000000000000000000, -5.322451846059955323E-30, 1.000000000000000000 ) ) ;
#299=LINE ( 'NONE', #1008, #2699 ) ;
#307=CARTESIAN_POINT ( 'NONE',  ( 1.000000000000000888, -4.257961476847964819E-29, 8.000000000000001776 ) ) ;
#308=AXIS2_PLACEMENT_3D ( 'NONE', #203, #4215, #7047 ) ;
#310=DIRECTION ( 'NONE',  ( 0.000000000000000000, 5.322451846059955323E-30, -1.000000000000000000 ) ) ;
#312=AXIS2_PLACEMENT_3D ( 'NONE', #6347, #6261, #6422 ) ;
#316=VERTEX_POINT ( 'NONE', #7169 ) ;
#319=VECTOR ( 'NONE', #7151, 1000.000000000000000 ) ;
#326=AXIS2_PLACEMENT_3D ( 'NONE', #7150, #8255, #3831 ) ;
#333=ORIENTED_EDGE ( 'NONE', *, *, #4840, .F. ) ;
#346=CARTESIAN_POINT ( 'NONE',  ( 10.40000000000001990, 0.000000000000000000, 4.440892098500626162E-13 ) ) ;
#350=PRODUCT_DEFINITION_FORMATION_WITH_SPECIFIED_SOURCE ( 'ANY', '', #5732, .NOT_KNOWN. ) ;
#354=ORIENTED_EDGE ( 'NONE', *, *, #6370, .T. ) ;
#367=VERTEX_POINT ( 'NONE', #1117 ) ;
#370=CARTESIAN_POINT ( 'NONE',  ( 1.521569672518448540E-45, 8.572527594031101439E-16, 7.000000000000000888 ) ) ;
#410=EDGE_CURVE ( 'NONE', #6592, #4707, #7950, .T. ) ;
#459=EDGE_LOOP ( 'NONE', ( #7143, #3679, #3302, #4348, #6214, #8113 ) ) ;
#463=CIRCLE ( 'NONE', #312, 5.000000000000069278 ) ;
#495=LINE ( 'NONE', #5274, #5177 ) ;
#496=CARTESIAN_POINT ( 'NONE',  ( 5.000000000000115463, 2.342598717236854977, -4.057500000000047180 ) ) ;
#521=ORIENTED_EDGE ( 'NONE', *, *, #8538, .T. ) ;
#529=EDGE_CURVE ( 'NONE', #7606, #3196, #1630, .T. ) ;
#541=CIRCLE ( 'NONE', #3878, 5.000000000000069278 ) ;
#546=DIRECTION ( 'NONE',  ( -1.000000000000000000, 1.774937036747276562E-30, 0.000000000000000000 ) ) ;
#561=AXIS2_PLACEMENT_3D ( 'NONE', #209, #4875, #2869 ) ;
#563=ORIENTED_EDGE ( 'NONE', *, *, #6140, .T. ) ;
#588=CARTESIAN_POINT ( 'NONE',  ( 5.000000000000004441, -4.685197434473812095, 0.000000000000000000 ) ) ;
#593=CARTESIAN_POINT ( 'NONE',  ( 10.40000000000001990, 6.123233995732941293E-16, -4.999999999999590550 ) ) ;
#598=AXIS2_PLACEMENT_3D ( 'NONE', #1093, #1261, #3795 ) ;
#608=EDGE_LOOP ( 'NONE', ( #1418, #8294, #5860, #146 ) ) ;
#617=ORIENTED_EDGE ( 'NONE', *, *, #410, .F. ) ;
#619=DIRECTION ( 'NONE',  ( 0.000000000000000000, -0.4999999999999989453, 0.8660254037844392627 ) ) ;
#632=EDGE_CURVE ( 'NONE', #6090, #6584, #2176, .T. ) ;
#652=ORIENTED_EDGE ( 'NONE', *, *, #8538, .F. ) ;
#699=CARTESIAN_POINT ( 'NONE',  ( 0.000000000000000000, -2.342598717236902939, 4.057500000000047180 ) ) ;
#706=ORIENTED_EDGE ( 'NONE', *, *, #1007, .T. ) ;
#758=VERTEX_POINT ( 'NONE', #8599 ) ;
#787=CARTESIAN_POINT ( 'NONE',  ( 5.000000000000004441, -3.513898075855406145, 2.028750000000023590 ) ) ;
#796=EDGE_CURVE ( 'NONE', #1068, #7820, #6319, .T. ) ;
#802=DIRECTION ( 'NONE',  ( -9.860761315262646473E-32, 0.4999999999999988898, -0.8660254037844392627 ) ) ;
#805=EDGE_CURVE ( 'NONE', #7820, #1068, #6328, .T. ) ;
#857=ORIENTED_EDGE ( 'NONE', *, *, #6152, .F. ) ;
#867=CARTESIAN_POINT ( 'NONE',  ( 0.000000000000000000, 4.685197434473812983, 0.000000000000000000 ) ) ;
#889=PLANE ( 'NONE',  #3626 ) ;
#919=CARTESIAN_POINT ( 'NONE',  ( 6.927742606685938292E-59, 3.903092032707603785E-29, -7.000000000000000888 ) ) ;
#928=ADVANCED_FACE ( 'NONE', ( #1563 ), #213, .T. ) ;
#935=CARTESIAN_POINT ( 'NONE',  ( 139.9999999999994316, 3.525609254162515373E-14, -4.172000000001442999 ) ) ;
#947=VERTEX_POINT ( 'NONE', #6980 ) ;
#962=ORIENTED_EDGE ( 'NONE', *, *, #796, .T. ) ;
#963=AXIS2_PLACEMENT_3D ( 'NONE', #1511, #3656, #291 ) ;
#964=EDGE_CURVE ( 'NONE', #7587, #6592, #5196, .T. ) ;
#965=ORIENTED_EDGE ( 'NONE', *, *, #7447, .T. ) ;
#984=AXIS2_PLACEMENT_3D ( 'NONE', #3097, #5790, #2658 ) ;
#1001=CARTESIAN_POINT ( 'NONE',  ( 0.000000000000000000, 4.685197434473812983, 0.000000000000000000 ) ) ;
#1007=EDGE_CURVE ( 'NONE', #4173, #282, #299, .T. ) ;
#1008=CARTESIAN_POINT ( 'NONE',  ( 5.000000000000004441, -4.685197434473812095, 0.000000000000000000 ) ) ;
#1013=VECTOR ( 'NONE', #3964, 1000.000000000000000 ) ;
#1033=PLANE ( 'NONE',  #1948 ) ;
#1047=PLANE ( 'NONE',  #561 ) ;
#1058=LINE ( 'NONE', #6898, #8106 ) ;
#1059=FACE_OUTER_BOUND ( 'NONE', #3912, .T. ) ;
#1068=VERTEX_POINT ( 'NONE', #919 ) ;
#1069=DIRECTION ( 'NONE',  ( 1.000000000000000000, -1.774937036747276562E-30, -9.447016907875728896E-60 ) ) ;
#1084=ORIENTED_EDGE ( 'NONE', *, *, #254, .T. ) ;
#1093=CARTESIAN_POINT ( 'NONE',  ( 5.000000000000004441, 0.000000000000000000, 0.000000000000000000 ) ) ;
#1108=ORIENTED_EDGE ( 'NONE', *, *, #2386, .T. ) ;
#1117=CARTESIAN_POINT ( 'NONE',  ( 10.00000000000001599, 2.945121478342286219E-29, -5.399999999999590905 ) ) ;
#1136=DIRECTION ( 'NONE',  ( 1.000000000000000000, -1.774937036747276562E-30, -9.447016907875728896E-60 ) ) ;
#1154=CARTESIAN_POINT ( 'NONE',  ( 5.000000000000004441, -2.159584836538827029E-29, 4.057500000000000107 ) ) ;
#1161=EDGE_CURVE ( 'NONE', #2145, #4173, #4390, .T. ) ;
#1182=LINE ( 'NONE', #3360, #5916 ) ;
#1189=DIRECTION ( 'NONE',  ( -3.451266460341926211E-31, 0.4999999999999985567, -0.8660254037844393737 ) ) ;
#1202=DIRECTION ( 'NONE',  ( 0.000000000000000000, -5.908893405598423146E-30, 1.000000000000000000 ) ) ;
#1261=DIRECTION ( 'NONE',  ( -1.000000000000000000, 1.774937036747276562E-30, 0.000000000000000000 ) ) ;
#1270=LINE ( 'NONE', #7327, #6124 ) ;
#1272=CARTESIAN_POINT ( 'NONE',  ( -31.74999999999994316, -1.972152263052529514E-28, 0.000000000000000000 ) ) ;
#1289=VECTOR ( 'NONE', #8334, 1000.000000000000114 ) ;
#1297=VECTOR ( 'NONE', #4764, 1000.000000000000114 ) ;
#1307=AXIS2_PLACEMENT_3D ( 'NONE', #3854, #546, #3204 ) ;
#1310=CARTESIAN_POINT ( 'NONE',  ( 0.000000000000000000, 4.685197434473812983, 0.000000000000000000 ) ) ;
#1321=EDGE_CURVE ( 'NONE', #4696, #7027, #2696, .T. ) ;
#1326=EDGE_LOOP ( 'NONE', ( #2945, #5668, #1084, #7460 ) ) ;
#1351=ORIENTED_EDGE ( 'NONE', *, *, #4273, .T. ) ;
#1357=ORIENTED_EDGE ( 'NONE', *, *, #7546, .F. ) ;
#1399=DIRECTION ( 'NONE',  ( -1.000000000000000000, 1.774937036747276562E-30, 0.000000000000000000 ) ) ;
#1405=DIRECTION ( 'NONE',  ( -3.328006943901143554E-30, 0.8660254037844380415, -0.5000000000000009992 ) ) ;
#1416=ORIENTED_EDGE ( 'NONE', *, *, #2113, .F. ) ;
#1418=ORIENTED_EDGE ( 'NONE', *, *, #3586, .F. ) ;
#1452=FACE_OUTER_BOUND ( 'NONE', #7790, .T. ) ;
#1453=PLANE ( 'NONE',  #7991 ) ;
#1455=ORIENTED_EDGE ( 'NONE', *, *, #6569, .T. ) ;
#1463=EDGE_LOOP ( 'NONE', ( #4568, #2280, #224 ) ) ;
#1464=DIRECTION ( 'NONE',  ( 0.000000000000000000, -5.322451846059955323E-30, 1.000000000000000000 ) ) ;
#1509=CARTESIAN_POINT ( 'NONE',  ( 5.000000000000004441, -4.685197434473812095, 0.000000000000000000 ) ) ;
#1511=CARTESIAN_POINT ( 'NONE',  ( 5.000000000000004441, 0.000000000000000000, 0.000000000000000000 ) ) ;
#1536=DIRECTION ( 'NONE',  ( -1.000000000000000000, 1.774937036747276562E-30, -0.000000000000000000 ) ) ;
#1544=FACE_OUTER_BOUND ( 'NONE', #1804, .T. ) ;
#1554=DIRECTION ( 'NONE',  ( 9.447016907875728896E-60, 5.322451846059955323E-30, -1.000000000000000000 ) ) ;
#1562=EDGE_CURVE ( 'NONE', #947, #2641, #7769, .T. ) ;
#1563=FACE_OUTER_BOUND ( 'NONE', #2568, .T. ) ;
#1604=DIRECTION ( 'NONE',  ( -1.000000000000000000, 1.774937036747276562E-30, 0.000000000000000000 ) ) ;
#1614=CIRCLE ( 'NONE', #7737, 5.000000000000034639 ) ;
#1622=ORIENTED_EDGE ( 'NONE', *, *, #3019, .T. ) ;
#1630=LINE ( 'NONE', #8267, #7893 ) ;
#1640=AXIS2_PLACEMENT_3D ( 'NONE', #5697, #4444, #310 ) ;
#1647=EDGE_CURVE ( 'NONE', #758, #8489, #1614, .T. ) ;
#1654=CLOSED_SHELL ( 'NONE', ( #6334, #4591, #3818, #7736, #928, #5279, #1681, #7675, #2447, #7657, #2866, #3977, #2237, #8322, #2513, #8157, #6528, #2882, #5191, #5542, #7300, #7524, #7608, #7983, #277, #3644, #5031 ) ) ;
#1668=ORIENTED_EDGE ( 'NONE', *, *, #3869, .T. ) ;
#1681=ADVANCED_FACE ( 'NONE', ( #7858, #5387 ), #3328, .T. ) ;
#1683=ORIENTED_EDGE ( 'NONE', *, *, #3717, .T. ) ;
#1726=DIRECTION ( 'NONE',  ( 3.451266460341926211E-31, -0.4999999999999985567, 0.8660254037844393737 ) ) ;
#1769=VERTEX_POINT ( 'NONE', #6097 ) ;
#1774=CARTESIAN_POINT ( 'NONE',  ( 5.000000000000004441, 0.000000000000000000, 0.000000000000000000 ) ) ;
#1784=DIRECTION ( 'NONE',  ( 1.774937036747276913E-30, -0.5000000000000014433, -0.8660254037844379305 ) ) ;
#1804=EDGE_LOOP ( 'NONE', ( #857, #8356, #4617 ) ) ;
#1805=CARTESIAN_POINT ( 'NONE',  ( 0.000000000000000000, 3.725716292241969286E-29, -7.000000000000000888 ) ) ;
#1824=LINE ( 'NONE', #7795, #319 ) ;
#1829=DIRECTION ( 'NONE',  ( 0.000000000000000000, 5.322451846059954622E-30, -1.000000000000000000 ) ) ;
#1875=DIRECTION ( 'NONE',  ( -1.774937036747276562E-30, 1.000000000000000000, -1.110768649713241713E-15 ) ) ;
#1885=DIRECTION ( 'NONE',  ( -1.000000000000000000, 1.774937036747276562E-30, 0.000000000000000000 ) ) ;
#1890=CARTESIAN_POINT ( 'NONE',  ( 0.000000000000000000, -4.685197434473812983, 0.000000000000000000 ) ) ;
#1929=EDGE_LOOP ( 'NONE', ( #7074, #35, #5212, #617 ) ) ;
#1948=AXIS2_PLACEMENT_3D ( 'NONE', #6351, #1069, #7075 ) ;
#1966=ORIENTED_EDGE ( 'NONE', *, *, #4642, .T. ) ;
#1971=CARTESIAN_POINT ( 'NONE',  ( 5.000000000000004441, 4.685197434473897360, 0.000000000000000000 ) ) ;
#1977=ORIENTED_EDGE ( 'NONE', *, *, #8268, .F. ) ;
#1999=VERTEX_POINT ( 'NONE', #6348 ) ;
#2013=PRODUCT_CONTEXT ( 'NONE', #5779, 'mechanical' ) ;
#2028=FACE_OUTER_BOUND ( 'NONE', #207, .T. ) ;
#2034=FACE_OUTER_BOUND ( 'NONE', #3215, .T. ) ;
#2052=VECTOR ( 'NONE', #5366, 1000.000000000000000 ) ;
#2091=AXIS2_PLACEMENT_3D ( 'NONE', #7338, #6604, #5389 ) ;
#2113=EDGE_CURVE ( 'NONE', #947, #2145, #1270, .T. ) ;
#2115=AXIS2_PLACEMENT_3D ( 'NONE', #5322, #5185, #7322 ) ;
#2118=ORIENTED_EDGE ( 'NONE', *, *, #3608, .F. ) ;
#2127=CARTESIAN_POINT ( 'NONE',  ( 10.00000000000000888, 0.000000000000000000, 4.440892098500626162E-13 ) ) ;
#2141=DIRECTION ( 'NONE',  ( -1.555753819465285427E-60, 1.110768649713241713E-15, 1.000000000000000000 ) ) ;
#2145=VERTEX_POINT ( 'NONE', #3185 ) ;
#2146=VECTOR ( 'NONE', #4165, 1000.000000000000000 ) ;
#2176=LINE ( 'NONE', #1509, #2146 ) ;
#2186=ORIENTED_EDGE ( 'NONE', *, *, #4471, .T. ) ;
#2190=CONICAL_SURFACE ( 'NONE', #7060, 4.057500000000000107, 1.047197551196592746 ) ;
#2211=DIRECTION ( 'NONE',  ( 0.000000000000000000, -5.322451846059954622E-30, 1.000000000000000000 ) ) ;
#2213=DIRECTION ( 'NONE',  ( 0.000000000000000000, -5.322451846059954622E-30, 1.000000000000000000 ) ) ;
#2220=DIRECTION ( 'NONE',  ( -1.000000000000000000, 1.774937036747276562E-30, 0.000000000000000000 ) ) ;
#2237=ADVANCED_FACE ( 'NONE', ( #1059 ), #4036, .T. ) ;
#2238=ORIENTED_EDGE ( 'NONE', *, *, #7447, .F. ) ;
#2254=DIRECTION ( 'NONE',  ( -0.7071067811864683028, -2.508471778025259936E-30, 0.7071067811866268427 ) ) ;
#2272=DIRECTION ( 'NONE',  ( -3.451266460341926211E-31, 0.4999999999999985567, -0.8660254037844393737 ) ) ;
#2280=ORIENTED_EDGE ( 'NONE', *, *, #7249, .T. ) ;
#2282=( GEOMETRIC_REPRESENTATION_CONTEXT ( 3 ) GLOBAL_UNCERTAINTY_ASSIGNED_CONTEXT ( ( #8368 ) ) GLOBAL_UNIT_ASSIGNED_CONTEXT ( ( #4544, #4499, #5198 ) ) REPRESENTATION_CONTEXT ( 'NONE', 'WORKASPACE' ) );
#2300=FACE_BOUND ( 'NONE', #6674, .T. ) ;
#2324=DIRECTION ( 'NONE',  ( 0.000000000000000000, -5.322451846059954622E-30, 1.000000000000000000 ) ) ;
#2333=( NAMED_UNIT ( * ) PLANE_ANGLE_UNIT ( ) SI_UNIT ( $, .RADIAN. ) );
#2364=PLANE ( 'NONE',  #7093 ) ;
#2367=ORIENTED_EDGE ( 'NONE', *, *, #632, .T. ) ;
#2372=AXIS2_PLACEMENT_3D ( 'NONE', #8142, #2141, #6662 ) ;
#2381=ORIENTED_EDGE ( 'NONE', *, *, #3717, .F. ) ;
#2386=EDGE_CURVE ( 'NONE', #316, #7714, #541, .T. ) ;
#2406=CIRCLE ( 'NONE', #598, 4.057500000000000107 ) ;
#2412=ORIENTED_EDGE ( 'NONE', *, *, #3154, .F. ) ;
#2447=ADVANCED_FACE ( 'NONE', ( #2675 ), #266, .T. ) ;
#2450=ORIENTED_EDGE ( 'NONE', *, *, #1562, .T. ) ;
#2453=CARTESIAN_POINT ( 'NONE',  ( 139.1719999999995423, 3.469446951953633753E-14, -1.443289932012703503E-12 ) ) ;
#2479=DIRECTION ( 'NONE',  ( 0.000000000000000000, -5.322451846059955323E-30, 1.000000000000000000 ) ) ;
#2493=EDGE_LOOP ( 'NONE', ( #1416, #2450, #5558, #521, #1455 ) ) ;
#2495=CARTESIAN_POINT ( 'NONE',  ( 5.000000000000004441, -2.342598717236951789, 4.057500000000047180 ) ) ;
#2497=AXIS2_PLACEMENT_3D ( 'NONE', #5703, #4371, #5556 ) ;
#2498=AXIS2_PLACEMENT_3D ( 'NONE', #3469, #6790, #6914 ) ;
#2513=ADVANCED_FACE ( 'NONE', ( #8122 ), #1453, .T. ) ;
#2546=EDGE_LOOP ( 'NONE', ( #6536, #1351, #563, #5959 ) ) ;
#2547=PRODUCT_DEFINITION_CONTEXT ( 'detailed design', #120, 'design' ) ;
#2560=FACE_OUTER_BOUND ( 'NONE', #2493, .T. ) ;
#2567=MECHANICAL_DESIGN_GEOMETRIC_PRESENTATION_REPRESENTATION('',(#5303),#6009);
#2568=EDGE_LOOP ( 'NONE', ( #1108, #2582, #5161, #5593 ) ) ;
#2573=CARTESIAN_POINT ( 'NONE',  ( 10.00000000000001599, 6.613092715395470808E-16, 5.400000000000479083 ) ) ;
#2575=CARTESIAN_POINT ( 'NONE',  ( 0.000000000000000000, 0.000000000000000000, 0.000000000000000000 ) ) ;
#2582=ORIENTED_EDGE ( 'NONE', *, *, #7597, .T. ) ;
#2590=LINE ( 'NONE', #1890, #6171 ) ;
#2593=DIRECTION ( 'NONE',  ( 1.885870601543981347E-30, -1.000000000000000000, 7.405124331421681105E-16 ) ) ;
#2609=LINE ( 'NONE', #699, #1013 ) ;
#2615=DIRECTION ( 'NONE',  ( -1.000000000000000000, 1.774937036747276562E-30, 0.000000000000000000 ) ) ;
#2617=ORIENTED_EDGE ( 'NONE', *, *, #3255, .F. ) ;
#2636=DIRECTION ( 'NONE',  ( 1.000000000000000000, -1.774937036747276562E-30, 0.000000000000000000 ) ) ;
#2638=LINE ( 'NONE', #4079, #3473 ) ;
#2641=VERTEX_POINT ( 'NONE', #6458 ) ;
#2644=CARTESIAN_POINT ( 'NONE',  ( 1.000000000000000888, 9.797174393176622763E-16, -8.000000000000001776 ) ) ;
#2658=DIRECTION ( 'NONE',  ( 0.000000000000000000, -5.908893405598423146E-30, 1.000000000000000000 ) ) ;
#2662=LINE ( 'NONE', #5316, #7018 ) ;
#2674=CARTESIAN_POINT ( 'NONE',  ( 1.630253220555408214E-45, 9.184850993604743653E-16, 7.000000000000000888 ) ) ;
#2675=FACE_OUTER_BOUND ( 'NONE', #608, .T. ) ;
#2678=EDGE_CURVE ( 'NONE', #8055, #5227, #4869, .T. ) ;
#2681=DIRECTION ( 'NONE',  ( 0.000000000000000000, -5.322451846059955323E-30, 1.000000000000000000 ) ) ;
#2696=LINE ( 'NONE', #5355, #6774 ) ;
#2699=VECTOR ( 'NONE', #4353, 1000.000000000000114 ) ;
#2724=ORIENTED_EDGE ( 'NONE', *, *, #8104, .T. ) ;
#2748=CARTESIAN_POINT ( 'NONE',  ( 10.40000000000001990, 0.000000000000000000, 4.440892098500626162E-13 ) ) ;
#2762=VERTEX_POINT ( 'NONE', #8101 ) ;
#2768=EDGE_LOOP ( 'NONE', ( #8360, #2617, #1966, #3991 ) ) ;
#2800=CARTESIAN_POINT ( 'NONE',  ( 10.40000000000001990, 2.874123996872394147E-29, -5.399999999999590905 ) ) ;
#2822=AXIS2_PLACEMENT_3D ( 'NONE', #7111, #1136, #7154 ) ;
#2866=ADVANCED_FACE ( 'NONE', ( #2300, #4397 ), #1047, .T. ) ;
#2869=DIRECTION ( 'NONE',  ( 0.000000000000000000, 5.322451846059955323E-30, -1.000000000000000000 ) ) ;
#2873=DIRECTION ( 'NONE',  ( -1.000000000000000000, 1.774937036747276562E-30, 0.000000000000000000 ) ) ;
#2878=CARTESIAN_POINT ( 'NONE',  ( 10.40000000000001990, 0.000000000000000000, 4.440892098500626162E-13 ) ) ;
#2882=ADVANCED_FACE ( 'NONE', ( #4219 ), #5038, .T. ) ;
#2906=FACE_OUTER_BOUND ( 'NONE', #2768, .T. ) ;
#2910=EDGE_LOOP ( 'NONE', ( #6899, #6956, #7499, #73 ) ) ;
#2926=AXIS2_PLACEMENT_3D ( 'NONE', #3575, #8181, #1726 ) ;
#2945=ORIENTED_EDGE ( 'NONE', *, *, #805, .F. ) ;
#2960=CARTESIAN_POINT ( 'NONE',  ( 5.000000000000004441, 0.000000000000000000, 0.000000000000000000 ) ) ;
#2991=VECTOR ( 'NONE', #8366, 1000.000000000000000 ) ;
#3017=FACE_OUTER_BOUND ( 'NONE', #46, .T. ) ;
#3019=EDGE_CURVE ( 'NONE', #2145, #282, #8002, .T. ) ;
#3023=DIRECTION ( 'NONE',  ( -1.000000000000000000, 1.774937036747276562E-30, 0.000000000000000000 ) ) ;
#3048=LINE ( 'NONE', #5736, #2991 ) ;
#3058=PRODUCT_DEFINITION_SHAPE ( 'NONE', 'NONE',  #5591 ) ;
#3065=ORIENTED_EDGE ( 'NONE', *, *, #5225, .F. ) ;
#3083=DIRECTION ( 'NONE',  ( -1.000000000000000000, 1.774937036747276562E-30, 0.000000000000000000 ) ) ;
#3097=CARTESIAN_POINT ( 'NONE',  ( 139.9999999999994316, 3.469446951953614189E-14, -1.443289932012703503E-12 ) ) ;
#3154=EDGE_CURVE ( 'NONE', #8100, #6175, #7314, .T. ) ;
#3173=EDGE_LOOP ( 'NONE', ( #962, #196 ) ) ;
#3176=EDGE_CURVE ( 'NONE', #79, #1769, #2609, .T. ) ;
#3185=CARTESIAN_POINT ( 'NONE',  ( 5.000000000000060396, -4.857225732735079428E-14, -4.057500000000047180 ) ) ;
#3196=VERTEX_POINT ( 'NONE', #787 ) ;
#3204=DIRECTION ( 'NONE',  ( 0.000000000000000000, -5.322451846059955323E-30, 1.000000000000000000 ) ) ;
#3208=CARTESIAN_POINT ( 'NONE',  ( 5.000000000000004441, 0.000000000000000000, 0.000000000000000000 ) ) ;
#3209=AXIS2_PLACEMENT_3D ( 'NONE', #6419, #8327, #1829 ) ;
#3210=CARTESIAN_POINT ( 'NONE',  ( 139.9999999999994316, 3.469446951953614189E-14, -1.443289932012703503E-12 ) ) ;
#3215=EDGE_LOOP ( 'NONE', ( #8526, #5947, #6571, #6313 ) ) ;
#3238=CYLINDRICAL_SURFACE ( 'NONE', #6588, 8.000000000000000000 ) ;
#3248=AXIS2_PLACEMENT_3D ( 'NONE', #6840, #6366, #2213 ) ;
#3255=EDGE_CURVE ( 'NONE', #8489, #758, #6169, .T. ) ;
#3302=ORIENTED_EDGE ( 'NONE', *, *, #4618, .T. ) ;
#3328=PLANE ( 'NONE',  #8306 ) ;
#3331=CIRCLE ( 'NONE', #3209, 5.400000000000034994 ) ;
#3332=CARTESIAN_POINT ( 'NONE',  ( -31.74999999999994316, -2.397948410737325939E-28, 8.000000000000000000 ) ) ;
#3359=DIRECTION ( 'NONE',  ( 1.774937036747276562E-30, 1.000000000000000000, -1.224646799147299959E-16 ) ) ;
#3360=CARTESIAN_POINT ( 'NONE',  ( 5.000000000000004441, -2.342598717236951789, 4.057500000000047180 ) ) ;
#3363=DIRECTION ( 'NONE',  ( -0.5000000000000042188, 1.060575238724958684E-16, -0.8660254037844361541 ) ) ;
#3372=VECTOR ( 'NONE', #619, 1000.000000000000000 ) ;
#3390=AXIS2_PLACEMENT_3D ( 'NONE', #2878, #5510, #4184 ) ;
#3392=CIRCLE ( 'NONE', #3248, 8.000000000000001776 ) ;
#3469=CARTESIAN_POINT ( 'NONE',  ( 5.000000000000115463, 7.027796151710889561, -4.057500000000047180 ) ) ;
#3473=VECTOR ( 'NONE', #2593, 1000.000000000000000 ) ;
#3480=AXIS2_PLACEMENT_3D ( 'NONE', #6864, #7636, #5517 ) ;
#3483=ORIENTED_EDGE ( 'NONE', *, *, #5225, .T. ) ;
#3498=ORIENTED_EDGE ( 'NONE', *, *, #529, .T. ) ;
#3512=DIRECTION ( 'NONE',  ( 1.000000000000000000, 0.000000000000000000, 0.000000000000000000 ) ) ;
#3520=FACE_OUTER_BOUND ( 'NONE', #6625, .T. ) ;
#3528=AXIS2_PLACEMENT_3D ( 'NONE', #2800, #220, #8156 ) ;
#3575=CARTESIAN_POINT ( 'NONE',  ( 5.000000000000004441, -4.685197434473812095, 0.000000000000000000 ) ) ;
#3576=ORIENTED_EDGE ( 'NONE', *, *, #222, .T. ) ;
#3582=EDGE_LOOP ( 'NONE', ( #1357, #4504 ) ) ;
#3586=EDGE_CURVE ( 'NONE', #5227, #7714, #495, .T. ) ;
#3602=CARTESIAN_POINT ( 'NONE',  ( 5.000000000000004441, 2.342598717236861638, 4.057500000000047180 ) ) ;
#3608=EDGE_CURVE ( 'NONE', #6850, #8100, #3973, .T. ) ;
#3624=AXIS2_PLACEMENT_3D ( 'NONE', #2127, #7433, #1464 ) ;
#3626=AXIS2_PLACEMENT_3D ( 'NONE', #225, #4110, #6778 ) ;
#3644=ADVANCED_FACE ( 'NONE', ( #4537 ), #5787, .F. ) ;
#3656=DIRECTION ( 'NONE',  ( -1.000000000000000000, 1.774937036747276562E-30, 0.000000000000000000 ) ) ;
#3662=VECTOR ( 'NONE', #1784, 999.9999999999998863 ) ;
#3679=ORIENTED_EDGE ( 'NONE', *, *, #3176, .F. ) ;
#3683=LINE ( 'NONE', #370, #1289 ) ;
#3685=ORIENTED_EDGE ( 'NONE', *, *, #5408, .F. ) ;
#3697=( NAMED_UNIT ( * ) SI_UNIT ( $, .STERADIAN. ) SOLID_ANGLE_UNIT ( ) );
#3717=EDGE_CURVE ( 'NONE', #1999, #5555, #8419, .T. ) ;
#3731=DIRECTION ( 'NONE',  ( 0.7071067811865474617, 2.508471778024696965E-30, -0.7071067811865474617 ) ) ;
#3737=CARTESIAN_POINT ( 'NONE',  ( 5.000000000000060396, -2.342598717236958006, -4.057500000000047180 ) ) ;
#3756=DIRECTION ( 'NONE',  ( 0.000000000000000000, -5.322451846059955323E-30, 1.000000000000000000 ) ) ;
#3769=CARTESIAN_POINT ( 'NONE',  ( 139.1719999999995423, 3.530679291910986181E-14, -5.000000000001512568 ) ) ;
#3795=DIRECTION ( 'NONE',  ( 0.000000000000000000, -5.322451846059955323E-30, 1.000000000000000000 ) ) ;
#3818=ADVANCED_FACE ( 'NONE', ( #4340 ), #5325, .T. ) ;
#3831=DIRECTION ( 'NONE',  ( 0.000000000000000000, -5.322451846059955323E-30, 1.000000000000000000 ) ) ;
#3843=CARTESIAN_POINT ( 'NONE',  ( -31.74999999999994316, 6.123233995735102772E-16, -5.000000000000034639 ) ) ;
#3853=CARTESIAN_POINT ( 'NONE',  ( 5.000000000000004441, 4.685197434473897360, 0.000000000000000000 ) ) ;
#3854=CARTESIAN_POINT ( 'NONE',  ( 5.000000000000004441, 0.000000000000000000, 0.000000000000000000 ) ) ;
#3868=EDGE_LOOP ( 'NONE', ( #4860, #5039, #4398, #5934, #4262 ) ) ;
#3869=EDGE_CURVE ( 'NONE', #1068, #18, #7043, .T. ) ;
#3878=AXIS2_PLACEMENT_3D ( 'NONE', #2453, #3023, #5102 ) ;
#3899=DIRECTION ( 'NONE',  ( -5.423418723394458790E-31, 0.8660254037844379305, -0.5000000000000014433 ) ) ;
#3912=EDGE_LOOP ( 'NONE', ( #7424, #4772, #1668, #6975 ) ) ;
#3916=CARTESIAN_POINT ( 'NONE',  ( 5.000000000000004441, 0.000000000000000000, 0.000000000000000000 ) ) ;
#3917=ORIENTED_EDGE ( 'NONE', *, *, #4884, .T. ) ;
#3918=VECTOR ( 'NONE', #5905, 1000.000000000000000 ) ;
#3928=CYLINDRICAL_SURFACE ( 'NONE', #5296, 8.000000000000000000 ) ;
#3936=TOROIDAL_SURFACE ( 'NONE', #3390, 5.400000000000034994, 0.4000000000000000222 ) ;
#3938=AXIS2_PLACEMENT_3D ( 'NONE', #8185, #1604, #5592 ) ;
#3964=DIRECTION ( 'NONE',  ( -1.774937036747276562E-30, 1.000000000000000000, -1.110768649713241713E-15 ) ) ;
#3969=EDGE_CURVE ( 'NONE', #6584, #2762, #2590, .T. ) ;
#3970=CARTESIAN_POINT ( 'NONE',  ( 5.000000000000004441, -2.342598717236951789, 4.057500000000047180 ) ) ;
#3973=LINE ( 'NONE', #4447, #3662 ) ;
#3976=CARTESIAN_POINT ( 'NONE',  ( 10.40000000000001990, 6.613092715395462920E-16, 5.400000000000479083 ) ) ;
#3977=ADVANCED_FACE ( 'NONE', ( #5963 ), #3238, .T. ) ;
#3991=ORIENTED_EDGE ( 'NONE', *, *, #8104, .F. ) ;
#4009=ORIENTED_EDGE ( 'NONE', *, *, #6314, .F. ) ;
#4028=DIRECTION ( 'NONE',  ( -1.000000000000000000, 1.774937036747276562E-30, 9.447016907875728896E-60 ) ) ;
#4036=CONICAL_SURFACE ( 'NONE', #1640, 7.000000000000000888, 0.7853981633974482790 ) ;
#4060=FACE_OUTER_BOUND ( 'NONE', #5214, .T. ) ;
#4077=CONICAL_SURFACE ( 'NONE', #5910, 4.057500000000000107, 1.047197551196592746 ) ;
#4079=CARTESIAN_POINT ( 'NONE',  ( 5.000000000000115463, 2.342598717236854977, -4.057500000000047180 ) ) ;
#4089=CIRCLE ( 'NONE', #1307, 4.057500000000000107 ) ;
#4110=DIRECTION ( 'NONE',  ( 1.000000000000000000, -1.774937036747276562E-30, -9.447016907875728896E-60 ) ) ;
#4131=PLANE ( 'NONE',  #2372 ) ;
#4165=DIRECTION ( 'NONE',  ( -1.000000000000000000, 1.774937036747276562E-30, 0.000000000000000000 ) ) ;
#4167=CARTESIAN_POINT ( 'NONE',  ( 139.9999999999994316, 3.469446951953611664E-14, 4.171999999998556419 ) ) ;
#4172=AXIS2_PLACEMENT_3D ( 'NONE', #3976, #3359, #5414 ) ;
#4173=VERTEX_POINT ( 'NONE', #8167 ) ;
#4184=DIRECTION ( 'NONE',  ( 9.447016907875728896E-60, 5.322451846059955323E-30, -1.000000000000000000 ) ) ;
#4193=VERTEX_POINT ( 'NONE', #2573 ) ;
#4201=DIRECTION ( 'NONE',  ( -1.774937036747276913E-30, 0.5000000000000014433, 0.8660254037844379305 ) ) ;
#4203=CARTESIAN_POINT ( 'NONE',  ( 0.000000000000000000, 0.000000000000000000, 0.000000000000000000 ) ) ;
#4215=DIRECTION ( 'NONE',  ( 1.000000000000000000, -1.774937036747276562E-30, -9.447016907875728896E-60 ) ) ;
#4219=FACE_OUTER_BOUND ( 'NONE', #7777, .T. ) ;
#4238=LINE ( 'NONE', #5741, #5033 ) ;
#4239=ORIENTED_EDGE ( 'NONE', *, *, #7249, .F. ) ;
#4262=ORIENTED_EDGE ( 'NONE', *, *, #6314, .T. ) ;
#4273=EDGE_CURVE ( 'NONE', #7714, #316, #463, .T. ) ;
#4289=LINE ( 'NONE', #3602, #6266 ) ;
#4296=DIRECTION ( 'NONE',  ( 1.000000000000000000, -1.774937036747276562E-30, 0.000000000000000000 ) ) ;
#4305=CIRCLE ( 'NONE', #963, 4.057500000000000107 ) ;
#4315=EDGE_CURVE ( 'NONE', #7820, #4707, #3683, .T. ) ;
#4317=VECTOR ( 'NONE', #5666, 1000.000000000000000 ) ;
#4320=VECTOR ( 'NONE', #6544, 999.9999999999998863 ) ;
#4337=LINE ( 'NONE', #3843, #4317 ) ;
#4338=EDGE_LOOP ( 'NONE', ( #3576, #2412, #2118, #5849, #4981 ) ) ;
#4340=FACE_OUTER_BOUND ( 'NONE', #1326, .T. ) ;
#4345=LINE ( 'NONE', #867, #4477 ) ;
#4348=ORIENTED_EDGE ( 'NONE', *, *, #3969, .T. ) ;
#4353=DIRECTION ( 'NONE',  ( -3.451266460341926211E-31, 0.4999999999999985567, -0.8660254037844393737 ) ) ;
#4360=VECTOR ( 'NONE', #4709, 1000.000000000000000 ) ;
#4362=EDGE_CURVE ( 'NONE', #7027, #1769, #5268, .T. ) ;
#4371=DIRECTION ( 'NONE',  ( -1.000000000000000000, 1.774937036747276562E-30, 0.000000000000000000 ) ) ;
#4378=DIRECTION ( 'NONE',  ( -1.000000000000000000, 1.774937036747276562E-30, 0.000000000000000000 ) ) ;
#4380=SHAPE_REPRESENTATION_RELATIONSHIP ( 'NONE' , 'NONE' ,  #83, #6359 ) ;
#4390=CIRCLE ( 'NONE', #7851, 4.057500000000000107 ) ;
#4393=AXIS2_PLACEMENT_3D ( 'NONE', #3853, #3899, #4201 ) ;
#4397=FACE_OUTER_BOUND ( 'NONE', #3582, .T. ) ;
#4398=ORIENTED_EDGE ( 'NONE', *, *, #1161, .T. ) ;
#4431=EDGE_CURVE ( 'NONE', #7587, #18, #2662, .T. ) ;
#4432=DIRECTION ( 'NONE',  ( 0.000000000000000000, -5.322451846059955323E-30, 1.000000000000000000 ) ) ;
#4444=DIRECTION ( 'NONE',  ( 1.000000000000000000, -1.774937036747276562E-30, 0.000000000000000000 ) ) ;
#4447=CARTESIAN_POINT ( 'NONE',  ( 5.000000000000004441, 4.685197434473897360, 0.000000000000000000 ) ) ;
#4471=EDGE_CURVE ( 'NONE', #3196, #6090, #1182, .T. ) ;
#4477=VECTOR ( 'NONE', #6277, 999.9999999999998863 ) ;
#4497=CARTESIAN_POINT ( 'NONE',  ( -31.74999999999994316, -1.972152263052529514E-28, 0.000000000000000000 ) ) ;
#4499=( NAMED_UNIT ( * ) PLANE_ANGLE_UNIT ( ) SI_UNIT ( $, .RADIAN. ) );
#4504=ORIENTED_EDGE ( 'NONE', *, *, #964, .F. ) ;
#4530=CARTESIAN_POINT ( 'NONE',  ( 5.000000000000115463, 2.342598717236854977, -4.057500000000047180 ) ) ;
#4537=FACE_OUTER_BOUND ( 'NONE', #1463, .T. ) ;
#4538=SHAPE_DEFINITION_REPRESENTATION ( #3058, #83 ) ;
#4544=( LENGTH_UNIT ( ) NAMED_UNIT ( * ) SI_UNIT ( .MILLI., .METRE. ) );
#4554=PLANE ( 'NONE',  #2091 ) ;
#4568=ORIENTED_EDGE ( 'NONE', *, *, #3608, .T. ) ;
#4591=ADVANCED_FACE ( 'NONE', ( #4060 ), #3936, .F. ) ;
#4617=ORIENTED_EDGE ( 'NONE', *, *, #69, .F. ) ;
#4618=EDGE_CURVE ( 'NONE', #79, #6584, #8194, .T. ) ;
#4642=EDGE_CURVE ( 'NONE', #8489, #367, #7283, .T. ) ;
#4654=CARTESIAN_POINT ( 'NONE',  ( 5.000000000000115463, 2.342598717236854977, -4.057500000000047180 ) ) ;
#4661=CARTESIAN_POINT ( 'NONE',  ( 5.000000000000004441, -2.342598717236951789, 4.057500000000047180 ) ) ;
#4682=DIRECTION ( 'NONE',  ( 0.000000000000000000, -5.322451846059955323E-30, 1.000000000000000000 ) ) ;
#4696=VERTEX_POINT ( 'NONE', #6938 ) ;
#4701=DIRECTION ( 'NONE',  ( -1.000000000000000000, 1.774937036747276562E-30, 0.000000000000000000 ) ) ;
#4707=VERTEX_POINT ( 'NONE', #307 ) ;
#4709=DIRECTION ( 'NONE',  ( 0.000000000000000000, -0.4999999999999989453, 0.8660254037844392627 ) ) ;
#4712=PLANE ( 'NONE',  #7975 ) ;
#4724=ORIENTED_EDGE ( 'NONE', *, *, #2678, .F. ) ;
#4732=CIRCLE ( 'NONE', #3624, 8.000000000000000000 ) ;
#4740=DIRECTION ( 'NONE',  ( -1.000000000000000000, 1.774937036747276562E-30, 0.000000000000000000 ) ) ;
#4755=DIRECTION ( 'NONE',  ( 0.000000000000000000, 5.322451846059955323E-30, -1.000000000000000000 ) ) ;
#4759=DIRECTION ( 'NONE',  ( -1.774937036747276212E-30, 0.5000000000000009992, 0.8660254037844380415 ) ) ;
#4764=DIRECTION ( 'NONE',  ( 1.774937036747276212E-30, -0.5000000000000009992, -0.8660254037844380415 ) ) ;
#4766=ORIENTED_EDGE ( 'NONE', *, *, #5764, .T. ) ;
#4772=ORIENTED_EDGE ( 'NONE', *, *, #796, .F. ) ;
#4783=ORIENTED_EDGE ( 'NONE', *, *, #4618, .F. ) ;
#4797=LINE ( 'NONE', #6078, #2052 ) ;
#4798=ORIENTED_EDGE ( 'NONE', *, *, #3019, .F. ) ;
#4832=DIRECTION ( 'NONE',  ( 1.000000000000000000, -1.774937036747276562E-30, 0.000000000000000000 ) ) ;
#4840=EDGE_CURVE ( 'NONE', #7606, #2641, #7837, .T. ) ;
#4843=ORIENTED_EDGE ( 'NONE', *, *, #7810, .T. ) ;
#4848=DIRECTION ( 'NONE',  ( 0.000000000000000000, 5.322451846059954622E-30, -1.000000000000000000 ) ) ;
#4860=ORIENTED_EDGE ( 'NONE', *, *, #1562, .F. ) ;
#4861=AXIS2_PLACEMENT_3D ( 'NONE', #7374, #7988, #7549 ) ;
#4869=CIRCLE ( 'NONE', #984, 4.171999999999999709 ) ;
#4875=DIRECTION ( 'NONE',  ( 1.000000000000000000, -1.774937036747276562E-30, -9.447016907875728896E-60 ) ) ;
#4884=EDGE_CURVE ( 'NONE', #282, #2762, #4797, .T. ) ;
#4898=AXIS2_PLACEMENT_3D ( 'NONE', #32, #6321, #2211 ) ;
#4979=FACE_OUTER_BOUND ( 'NONE', #6769, .T. ) ;
#4981=ORIENTED_EDGE ( 'NONE', *, *, #1321, .T. ) ;
#5001=CIRCLE ( 'NONE', #2497, 4.171999999999999709 ) ;
#5012=CARTESIAN_POINT ( 'NONE',  ( 139.9999999999994316, 3.469446951953611664E-14, 4.171999999998556419 ) ) ;
#5017=PLANE ( 'NONE',  #3480 ) ;
#5021=ORIENTED_EDGE ( 'NONE', *, *, #5408, .T. ) ;
#5031=ADVANCED_FACE ( 'NONE', ( #2560 ), #2190, .F. ) ;
#5032=( LENGTH_UNIT ( ) NAMED_UNIT ( * ) SI_UNIT ( .MILLI., .METRE. ) );
#5033=VECTOR ( 'NONE', #7712, 1000.000000000000000 ) ;
#5038=PLANE ( 'NONE',  #2926 ) ;
#5039=ORIENTED_EDGE ( 'NONE', *, *, #2113, .T. ) ;
#5100=EDGE_LOOP ( 'NONE', ( #5495, #6333, #4766, #1683, #965 ) ) ;
#5101=CARTESIAN_POINT ( 'NONE',  ( 10.00000000000000888, 9.797174393176348634E-16, -7.999999999999555911 ) ) ;
#5102=DIRECTION ( 'NONE',  ( 0.000000000000000000, -4.930380657631255821E-30, 1.000000000000000000 ) ) ;
#5107=ORIENTED_EDGE ( 'NONE', *, *, #4840, .T. ) ;
#5161=ORIENTED_EDGE ( 'NONE', *, *, #3255, .T. ) ;
#5177=VECTOR ( 'NONE', #7755, 1000.000000000000000 ) ;
#5185=DIRECTION ( 'NONE',  ( -1.000000000000000000, 1.774937036747276562E-30, 0.000000000000000000 ) ) ;
#5191=ADVANCED_FACE ( 'NONE', ( #3017 ), #5017, .F. ) ;
#5196=CIRCLE ( 'NONE', #5642, 8.000000000000000000 ) ;
#5198=( NAMED_UNIT ( * ) SI_UNIT ( $, .STERADIAN. ) SOLID_ANGLE_UNIT ( ) );
#5212=ORIENTED_EDGE ( 'NONE', *, *, #254, .F. ) ;
#5214=EDGE_LOOP ( 'NONE', ( #5680, #7409, #3065, #6663 ) ) ;
#5225=EDGE_CURVE ( 'NONE', #367, #4193, #7781, .T. ) ;
#5227=VERTEX_POINT ( 'NONE', #935 ) ;
#5235=EDGE_CURVE ( 'NONE', #5227, #8055, #5001, .T. ) ;
#5268=LINE ( 'NONE', #1310, #4360 ) ;
#5274=CARTESIAN_POINT ( 'NONE',  ( 139.9999999999994316, 3.520539216414043934E-14, -4.172000000001442999 ) ) ;
#5279=ADVANCED_FACE ( 'NONE', ( #2034 ), #8069, .T. ) ;
#5285=LINE ( 'NONE', #1971, #4320 ) ;
#5296=AXIS2_PLACEMENT_3D ( 'NONE', #1272, #1885, #4682 ) ;
#5300=FACE_OUTER_BOUND ( 'NONE', #4338, .T. ) ;
#5303=STYLED_ITEM('',(#8670),#5864);
#5311=DIRECTION ( 'NONE',  ( -1.774937036747276562E-30, 1.000000000000000000, -1.110768649713241713E-15 ) ) ;
#5316=CARTESIAN_POINT ( 'NONE',  ( -31.74999999999994316, 9.797174393177281462E-16, -8.000000000000000000 ) ) ;
#5322=CARTESIAN_POINT ( 'NONE',  ( 5.000000000000004441, 0.000000000000000000, 0.000000000000000000 ) ) ;
#5325=CONICAL_SURFACE ( 'NONE', #5622, 7.000000000000000888, 0.7853981633974482790 ) ;
#5355=CARTESIAN_POINT ( 'NONE',  ( 5.000000000000004441, 4.685197434473897360, 0.000000000000000000 ) ) ;
#5366=DIRECTION ( 'NONE',  ( -1.000000000000000000, 1.774937036747276562E-30, 0.000000000000000000 ) ) ;
#5387=FACE_OUTER_BOUND ( 'NONE', #3173, .T. ) ;
#5389=DIRECTION ( 'NONE',  ( 0.000000000000000000, 5.322451846059955323E-30, -1.000000000000000000 ) ) ;
#5408=EDGE_CURVE ( 'NONE', #7606, #79, #3048, .T. ) ;
#5414=DIRECTION ( 'NONE',  ( 0.000000000000000000, 1.224646799147300206E-16, 1.000000000000000000 ) ) ;
#5495=ORIENTED_EDGE ( 'NONE', *, *, #4362, .F. ) ;
#5498=LINE ( 'NONE', #8147, #137 ) ;
#5510=DIRECTION ( 'NONE',  ( 1.000000000000000000, -1.774937036747276562E-30, 0.000000000000000000 ) ) ;
#5517=DIRECTION ( 'NONE',  ( -1.885870601543981347E-30, 1.000000000000000000, -7.405124331421681105E-16 ) ) ;
#5523=VECTOR ( 'NONE', #8391, 1000.000000000000114 ) ;
#5542=ADVANCED_FACE ( 'NONE', ( #5300 ), #7212, .F. ) ;
#5555=VERTEX_POINT ( 'NONE', #148 ) ;
#5556=DIRECTION ( 'NONE',  ( 0.000000000000000000, -5.908893405598423146E-30, 1.000000000000000000 ) ) ;
#5558=ORIENTED_EDGE ( 'NONE', *, *, #6968, .T. ) ;
#5585=CIRCLE ( 'NONE', #4172, 0.4000000000000001887 ) ;
#5591=PRODUCT_DEFINITION ( 'UNKNOWN', '', #350, #2547 ) ;
#5592=DIRECTION ( 'NONE',  ( 0.000000000000000000, -5.322451846059954622E-30, 1.000000000000000000 ) ) ;
#5593=ORIENTED_EDGE ( 'NONE', *, *, #6140, .F. ) ;
#5614=CIRCLE ( 'NONE', #4898, 8.000000000000001776 ) ;
#5622=AXIS2_PLACEMENT_3D ( 'NONE', #6960, #4296, #8305 ) ;
#5642=AXIS2_PLACEMENT_3D ( 'NONE', #7622, #2220, #6933 ) ;
#5658=CARTESIAN_POINT ( 'NONE',  ( 10.00000000000000888, 0.000000000000000000, 4.440892098500626162E-13 ) ) ;
#5666=DIRECTION ( 'NONE',  ( -1.000000000000000000, 1.774937036747276562E-30, 0.000000000000000000 ) ) ;
#5668=ORIENTED_EDGE ( 'NONE', *, *, #4315, .T. ) ;
#5680=ORIENTED_EDGE ( 'NONE', *, *, #1647, .F. ) ;
#5697=CARTESIAN_POINT ( 'NONE',  ( 0.000000000000000000, 0.000000000000000000, 0.000000000000000000 ) ) ;
#5703=CARTESIAN_POINT ( 'NONE',  ( 139.9999999999994316, 3.469446951953614189E-14, -1.443289932012703503E-12 ) ) ;
#5732=PRODUCT ( 'socket head cap screw_am_B18.3.1M - 10 x 1.5 x 130 Hex SHCS -- 32NHX', 'socket head cap screw_am_B18.3.1M - 10 x 1.5 x 130 Hex SHCS -- 32NHX', '', ( #2013 ) ) ;
#5736=CARTESIAN_POINT ( 'NONE',  ( 5.000000000000004441, -2.342598717236951789, 4.057500000000047180 ) ) ;
#5738=EDGE_CURVE ( 'NONE', #758, #4193, #5585, .T. ) ;
#5741=CARTESIAN_POINT ( 'NONE',  ( -31.74999999999994316, -2.238274855355529073E-28, 5.000000000000034639 ) ) ;
#5764=EDGE_CURVE ( 'NONE', #4696, #1999, #5498, .T. ) ;
#5779=APPLICATION_CONTEXT ( 'automotive_design' ) ;
#5787=PLANE ( 'NONE',  #2822 ) ;
#5790=DIRECTION ( 'NONE',  ( -1.000000000000000000, 1.774937036747276562E-30, 0.000000000000000000 ) ) ;
#5849=ORIENTED_EDGE ( 'NONE', *, *, #7810, .F. ) ;
#5860=ORIENTED_EDGE ( 'NONE', *, *, #208, .T. ) ;
#5863=DIRECTION ( 'NONE',  ( -1.000000000000000000, 1.774937036747276562E-30, 0.000000000000000000 ) ) ;
#5864=MANIFOLD_SOLID_BREP ( 'Hex', #1654 ) ;
#5905=DIRECTION ( 'NONE',  ( -1.000000000000000000, 1.774937036747276562E-30, 0.000000000000000000 ) ) ;
#5910=AXIS2_PLACEMENT_3D ( 'NONE', #3916, #2615, #3756 ) ;
#5911=AXIS2_PLACEMENT_3D ( 'NONE', #2575, #5863, #2479 ) ;
#5916=VECTOR ( 'NONE', #7197, 1000.000000000000114 ) ;
#5934=ORIENTED_EDGE ( 'NONE', *, *, #69, .T. ) ;
#5945=ORIENTED_EDGE ( 'NONE', *, *, #6968, .F. ) ;
#5947=ORIENTED_EDGE ( 'NONE', *, *, #3586, .T. ) ;
#5957=FACE_OUTER_BOUND ( 'NONE', #1929, .T. ) ;
#5959=ORIENTED_EDGE ( 'NONE', *, *, #1647, .T. ) ;
#5963=FACE_OUTER_BOUND ( 'NONE', #2910, .T. ) ;
#5998=AXIS2_PLACEMENT_3D ( 'NONE', #3210, #4740, #1202 ) ;
#6004=EDGE_LOOP ( 'NONE', ( #4783, #3685, #3498, #2186, #2367 ) ) ;
#6009=( GEOMETRIC_REPRESENTATION_CONTEXT ( 3 ) GLOBAL_UNCERTAINTY_ASSIGNED_CONTEXT ( ( #7441 ) ) GLOBAL_UNIT_ASSIGNED_CONTEXT ( ( #5032, #2333, #3697 ) ) REPRESENTATION_CONTEXT ( 'NONE', 'WORKASPACE' ) );
#6011=DIRECTION ( 'NONE',  ( 0.000000000000000000, -5.322451846059955323E-30, 1.000000000000000000 ) ) ;
#6040=VECTOR ( 'NONE', #8551, 1000.000000000000000 ) ;
#6069=CARTESIAN_POINT ( 'NONE',  ( 5.000000000000115463, 3.513898075855330205, -2.028750000000023590 ) ) ;
#6078=CARTESIAN_POINT ( 'NONE',  ( 5.000000000000060396, -2.342598717236958006, -4.057500000000047180 ) ) ;
#6090=VERTEX_POINT ( 'NONE', #588 ) ;
#6097=CARTESIAN_POINT ( 'NONE',  ( 0.000000000000000000, 2.342598717236902939, 4.057500000000047180 ) ) ;
#6124=VECTOR ( 'NONE', #3363, 1000.000000000000114 ) ;
#6140=EDGE_CURVE ( 'NONE', #316, #758, #4238, .T. ) ;
#6152=EDGE_CURVE ( 'NONE', #6090, #4173, #1058, .T. ) ;
#6169=CIRCLE ( 'NONE', #6855, 5.000000000000034639 ) ;
#6171=VECTOR ( 'NONE', #1189, 1000.000000000000114 ) ;
#6175=VERTEX_POINT ( 'NONE', #7672 ) ;
#6195=PLANE ( 'NONE',  #308 ) ;
#6214=ORIENTED_EDGE ( 'NONE', *, *, #6370, .F. ) ;
#6231=DIRECTION ( 'NONE',  ( 1.774937036747276212E-30, -0.5000000000000009992, -0.8660254037844380415 ) ) ;
#6244=CARTESIAN_POINT ( 'NONE',  ( 0.000000000000000000, -4.685197434473812983, 0.000000000000000000 ) ) ;
#6261=DIRECTION ( 'NONE',  ( -1.000000000000000000, 1.774937036747276562E-30, 0.000000000000000000 ) ) ;
#6266=VECTOR ( 'NONE', #7601, 1000.000000000000000 ) ;
#6277=DIRECTION ( 'NONE',  ( 1.774937036747276913E-30, -0.5000000000000014433, -0.8660254037844379305 ) ) ;
#6282=ORIENTED_EDGE ( 'NONE', *, *, #5764, .F. ) ;
#6313=ORIENTED_EDGE ( 'NONE', *, *, #208, .F. ) ;
#6314=EDGE_CURVE ( 'NONE', #3196, #2641, #2406, .T. ) ;
#6319=CIRCLE ( 'NONE', #326, 7.000000000000000888 ) ;
#6321=DIRECTION ( 'NONE',  ( -1.000000000000000000, 1.774937036747276562E-30, 0.000000000000000000 ) ) ;
#6328=CIRCLE ( 'NONE', #5911, 7.000000000000000888 ) ;
#6333=ORIENTED_EDGE ( 'NONE', *, *, #1321, .F. ) ;
#6334=ADVANCED_FACE ( 'NONE', ( #6416 ), #4077, .F. ) ;
#6347=CARTESIAN_POINT ( 'NONE',  ( 139.1719999999995423, 3.469446951953633753E-14, -1.443289932012703503E-12 ) ) ;
#6348=CARTESIAN_POINT ( 'NONE',  ( 5.000000000000004441, 3.513898075855358627, 2.028750000000023590 ) ) ;
#6351=CARTESIAN_POINT ( 'NONE',  ( 5.000000000000115463, 7.027796151710889561, -4.057500000000047180 ) ) ;
#6359=ADVANCED_BREP_SHAPE_REPRESENTATION ( '', ( #5864, #7563 ), #2282 ) ;
#6366=DIRECTION ( 'NONE',  ( -1.000000000000000000, 1.774937036747276562E-30, 0.000000000000000000 ) ) ;
#6370=EDGE_CURVE ( 'NONE', #6175, #2762, #1824, .T. ) ;
#6389=DIRECTION ( 'NONE',  ( 0.000000000000000000, 5.322451846059955323E-30, -1.000000000000000000 ) ) ;
#6416=FACE_OUTER_BOUND ( 'NONE', #3868, .T. ) ;
#6419=CARTESIAN_POINT ( 'NONE',  ( 10.00000000000000888, 0.000000000000000000, 4.440892098500626162E-13 ) ) ;
#6422=DIRECTION ( 'NONE',  ( 0.000000000000000000, -4.930380657631255821E-30, 1.000000000000000000 ) ) ;
#6425=DIRECTION ( 'NONE',  ( 1.000000000000000000, -1.774937036747276562E-30, -9.447016907875728896E-60 ) ) ;
#6458=CARTESIAN_POINT ( 'NONE',  ( 5.000000000000004441, -4.163336342344337027E-14, 4.057500000000047180 ) ) ;
#6506=CARTESIAN_POINT ( 'NONE',  ( -31.74999999999994316, -1.972152263052529514E-28, 0.000000000000000000 ) ) ;
#6528=ADVANCED_FACE ( 'NONE', ( #7408 ), #4712, .T. ) ;
#6536=ORIENTED_EDGE ( 'NONE', *, *, #7597, .F. ) ;
#6544=DIRECTION ( 'NONE',  ( 1.774937036747276913E-30, -0.5000000000000014433, -0.8660254037844379305 ) ) ;
#6549=ORIENTED_EDGE ( 'NONE', *, *, #4884, .F. ) ;
#6569=EDGE_CURVE ( 'NONE', #6850, #2145, #8197, .T. ) ;
#6571=ORIENTED_EDGE ( 'NONE', *, *, #2386, .F. ) ;
#6584=VERTEX_POINT ( 'NONE', #6244 ) ;
#6585=CARTESIAN_POINT ( 'NONE',  ( 5.000000000000004441, 4.685197434473897360, 0.000000000000000000 ) ) ;
#6588=AXIS2_PLACEMENT_3D ( 'NONE', #6506, #7855, #2681 ) ;
#6592=VERTEX_POINT ( 'NONE', #7539 ) ;
#6604=DIRECTION ( 'NONE',  ( 1.000000000000000000, -1.774937036747276562E-30, -9.447016907875728896E-60 ) ) ;
#6619=FACE_OUTER_BOUND ( 'NONE', #8018, .T. ) ;
#6625=EDGE_LOOP ( 'NONE', ( #6282, #4843, #652 ) ) ;
#6662=DIRECTION ( 'NONE',  ( 1.774937036747276562E-30, -1.000000000000000000, 1.110768649713241713E-15 ) ) ;
#6663=ORIENTED_EDGE ( 'NONE', *, *, #4642, .F. ) ;
#6674=EDGE_LOOP ( 'NONE', ( #3483, #2724 ) ) ;
#6741=CARTESIAN_POINT ( 'NONE',  ( 10.40000000000001990, 0.000000000000000000, 4.440892098500626162E-13 ) ) ;
#6753=VECTOR ( 'NONE', #5311, 1000.000000000000000 ) ;
#6769=EDGE_LOOP ( 'NONE', ( #4724, #7181 ) ) ;
#6774=VECTOR ( 'NONE', #4701, 1000.000000000000000 ) ;
#6777=ORIENTED_EDGE ( 'NONE', *, *, #3176, .T. ) ;
#6778=DIRECTION ( 'NONE',  ( 0.000000000000000000, 5.322451846059955323E-30, -1.000000000000000000 ) ) ;
#6779=CARTESIAN_POINT ( 'NONE',  ( 5.000000000000004441, 4.685197434473897360, 0.000000000000000000 ) ) ;
#6790=DIRECTION ( 'NONE',  ( 1.000000000000000000, -1.774937036747276562E-30, -9.447016907875728896E-60 ) ) ;
#6820=DIRECTION ( 'NONE',  ( -5.473822126268816683E-48, -0.8660254037844392627, -0.4999999999999988898 ) ) ;
#6840=CARTESIAN_POINT ( 'NONE',  ( 1.000000000000000888, 0.000000000000000000, 0.000000000000000000 ) ) ;
#6845=DIRECTION ( 'NONE',  ( 0.000000000000000000, -0.4999999999999989453, 0.8660254037844392627 ) ) ;
#6850=VERTEX_POINT ( 'NONE', #6069 ) ;
#6855=AXIS2_PLACEMENT_3D ( 'NONE', #2748, #4832, #4755 ) ;
#6864=CARTESIAN_POINT ( 'NONE',  ( 5.000000000000115463, 2.342598717236854977, -4.057500000000047180 ) ) ;
#6879=VECTOR ( 'NONE', #3731, 1000.000000000000114 ) ;
#6898=CARTESIAN_POINT ( 'NONE',  ( 5.000000000000004441, -4.685197434473812095, 0.000000000000000000 ) ) ;
#6899=ORIENTED_EDGE ( 'NONE', *, *, #4431, .F. ) ;
#6914=DIRECTION ( 'NONE',  ( 0.000000000000000000, 5.322451846059955323E-30, -1.000000000000000000 ) ) ;
#6933=DIRECTION ( 'NONE',  ( 0.000000000000000000, -5.322451846059955323E-30, 1.000000000000000000 ) ) ;
#6938=CARTESIAN_POINT ( 'NONE',  ( 5.000000000000004441, 4.685197434473897360, 0.000000000000000000 ) ) ;
#6956=ORIENTED_EDGE ( 'NONE', *, *, #964, .T. ) ;
#6960=CARTESIAN_POINT ( 'NONE',  ( 0.000000000000000000, 0.000000000000000000, 0.000000000000000000 ) ) ;
#6968=EDGE_CURVE ( 'NONE', #2641, #1999, #4305, .T. ) ;
#6975=ORIENTED_EDGE ( 'NONE', *, *, #8357, .T. ) ;
#6980=CARTESIAN_POINT ( 'NONE',  ( 7.342598717236914041, 0.000000000000000000, 0.000000000000000000 ) ) ;
#7013=DIRECTION ( 'NONE',  ( 1.000000000000000000, -1.774937036747276562E-30, 0.000000000000000000 ) ) ;
#7018=VECTOR ( 'NONE', #1399, 1000.000000000000000 ) ;
#7020=DIRECTION ( 'NONE',  ( 0.000000000000000000, -5.322451846059955323E-30, 1.000000000000000000 ) ) ;
#7027=VERTEX_POINT ( 'NONE', #1001 ) ;
#7043=LINE ( 'NONE', #1805, #6879 ) ;
#7047=DIRECTION ( 'NONE',  ( 0.000000000000000000, 5.322451846059955323E-30, -1.000000000000000000 ) ) ;
#7060=AXIS2_PLACEMENT_3D ( 'NONE', #3208, #7304, #7957 ) ;
#7074=ORIENTED_EDGE ( 'NONE', *, *, #7546, .T. ) ;
#7075=DIRECTION ( 'NONE',  ( 0.000000000000000000, 5.322451846059955323E-30, -1.000000000000000000 ) ) ;
#7093=AXIS2_PLACEMENT_3D ( 'NONE', #7642, #6425, #6389 ) ;
#7111=CARTESIAN_POINT ( 'NONE',  ( 5.000000000000115463, 7.027796151710889561, -4.057500000000047180 ) ) ;
#7143=ORIENTED_EDGE ( 'NONE', *, *, #4362, .T. ) ;
#7150=CARTESIAN_POINT ( 'NONE',  ( 0.000000000000000000, 0.000000000000000000, 0.000000000000000000 ) ) ;
#7151=DIRECTION ( 'NONE',  ( 1.885870601543981347E-30, -1.000000000000000000, 7.405124331421681105E-16 ) ) ;
#7154=DIRECTION ( 'NONE',  ( 0.000000000000000000, 5.322451846059955323E-30, -1.000000000000000000 ) ) ;
#7169=CARTESIAN_POINT ( 'NONE',  ( 139.1719999999995423, 3.469446951953611664E-14, 4.999999999998625988 ) ) ;
#7181=ORIENTED_EDGE ( 'NONE', *, *, #5235, .F. ) ;
#7197=DIRECTION ( 'NONE',  ( 1.774937036747276212E-30, -0.5000000000000009992, -0.8660254037844380415 ) ) ;
#7207=AXIS2_PLACEMENT_3D ( 'NONE', #2960, #2873, #7020 ) ;
#7212=PLANE ( 'NONE',  #4393 ) ;
#7224=ORIENTED_EDGE ( 'NONE', *, *, #8268, .T. ) ;
#7247=ORIENTED_EDGE ( 'NONE', *, *, #1007, .F. ) ;
#7249=EDGE_CURVE ( 'NONE', #8100, #2145, #2638, .T. ) ;
#7283=CIRCLE ( 'NONE', #3528, 0.4000000000000001887 ) ;
#7292=ORIENTED_EDGE ( 'NONE', *, *, #3154, .T. ) ;
#7300=ADVANCED_FACE ( 'NONE', ( #2028 ), #4554, .F. ) ;
#7304=DIRECTION ( 'NONE',  ( -1.000000000000000000, 1.774937036747276562E-30, 0.000000000000000000 ) ) ;
#7314=LINE ( 'NONE', #4530, #3918 ) ;
#7322=DIRECTION ( 'NONE',  ( 0.000000000000000000, -5.322451846059955323E-30, 1.000000000000000000 ) ) ;
#7327=CARTESIAN_POINT ( 'NONE',  ( 5.000000000000004441, 4.969004387540602357E-16, -4.057500000000000107 ) ) ;
#7331=EDGE_LOOP ( 'NONE', ( #7895, #5107, #4009 ) ) ;
#7338=CARTESIAN_POINT ( 'NONE',  ( 5.000000000000115463, 7.027796151710889561, -4.057500000000047180 ) ) ;
#7350=LINE ( 'NONE', #4661, #6753 ) ;
#7374=CARTESIAN_POINT ( 'NONE',  ( 139.9999999999994316, 3.469446951953614189E-14, -1.443289932012703503E-12 ) ) ;
#7378=VECTOR ( 'NONE', #8093, 1000.000000000000000 ) ;
#7401=VECTOR ( 'NONE', #2254, 1000.000000000000000 ) ;
#7408=FACE_OUTER_BOUND ( 'NONE', #6004, .T. ) ;
#7409=ORIENTED_EDGE ( 'NONE', *, *, #5738, .T. ) ;
#7424=ORIENTED_EDGE ( 'NONE', *, *, #4315, .F. ) ;
#7433=DIRECTION ( 'NONE',  ( -1.000000000000000000, 1.774937036747276562E-30, 0.000000000000000000 ) ) ;
#7441=UNCERTAINTY_MEASURE_WITH_UNIT (LENGTH_MEASURE( 1.000000000000000082E-05 ), #5032, 'distance_accuracy_value', 'NONE');
#7447=EDGE_CURVE ( 'NONE', #5555, #1769, #4289, .T. ) ;
#7460=ORIENTED_EDGE ( 'NONE', *, *, #3869, .F. ) ;
#7478=DIRECTION ( 'NONE',  ( 0.000000000000000000, 0.000000000000000000, 1.000000000000000000 ) ) ;
#7499=ORIENTED_EDGE ( 'NONE', *, *, #410, .T. ) ;
#7524=ADVANCED_FACE ( 'NONE', ( #1544 ), #8215, .F. ) ;
#7539=CARTESIAN_POINT ( 'NONE',  ( 10.00000000000000888, -4.257961476847964258E-29, 8.000000000000444089 ) ) ;
#7546=EDGE_CURVE ( 'NONE', #6592, #7587, #4732, .T. ) ;
#7549=DIRECTION ( 'NONE',  ( 0.000000000000000000, -5.908893405598423146E-30, 1.000000000000000000 ) ) ;
#7563=AXIS2_PLACEMENT_3D ( 'NONE', #4203, #7478, #3512 ) ;
#7571=LINE ( 'NONE', #4167, #7401 ) ;
#7582=ORIENTED_EDGE ( 'NONE', *, *, #3969, .F. ) ;
#7587=VERTEX_POINT ( 'NONE', #5101 ) ;
#7597=EDGE_CURVE ( 'NONE', #7714, #8489, #4337, .T. ) ;
#7601=DIRECTION ( 'NONE',  ( -1.000000000000000000, 1.774937036747276562E-30, 0.000000000000000000 ) ) ;
#7606=VERTEX_POINT ( 'NONE', #2495 ) ;
#7608=ADVANCED_FACE ( 'NONE', ( #8381 ), #1033, .F. ) ;
#7609=TOROIDAL_SURFACE ( 'NONE', #8028, 5.400000000000034994, 0.4000000000000000222 ) ;
#7622=CARTESIAN_POINT ( 'NONE',  ( 10.00000000000000888, 0.000000000000000000, 4.440892098500626162E-13 ) ) ;
#7636=DIRECTION ( 'NONE',  ( 2.644781493090985226E-59, -7.405124331421681105E-16, -1.000000000000000000 ) ) ;
#7642=CARTESIAN_POINT ( 'NONE',  ( 139.9999999999996305, 4.171999999999862929, -1.443289932012703503E-12 ) ) ;
#7657=ADVANCED_FACE ( 'NONE', ( #7685 ), #7804, .T. ) ;
#7672=CARTESIAN_POINT ( 'NONE',  ( 1.110223024625156540E-13, 2.342598717236896722, -4.057500000000047180 ) ) ;
#7675=ADVANCED_FACE ( 'NONE', ( #4979 ), #2364, .T. ) ;
#7685=FACE_OUTER_BOUND ( 'NONE', #2546, .T. ) ;
#7700=ORIENTED_EDGE ( 'NONE', *, *, #6152, .T. ) ;
#7712=DIRECTION ( 'NONE',  ( -1.000000000000000000, 1.774937036747276562E-30, 0.000000000000000000 ) ) ;
#7714=VERTEX_POINT ( 'NONE', #3769 ) ;
#7736=ADVANCED_FACE ( 'NONE', ( #5957 ), #3928, .T. ) ;
#7737=AXIS2_PLACEMENT_3D ( 'NONE', #6741, #2636, #8506 ) ;
#7755=DIRECTION ( 'NONE',  ( -0.7071067811864683028, 8.659560562356407042E-17, -0.7071067811866268427 ) ) ;
#7769=LINE ( 'NONE', #1154, #5523 ) ;
#7777=EDGE_LOOP ( 'NONE', ( #7582, #8230, #7700, #706, #3917 ) ) ;
#7781=CIRCLE ( 'NONE', #8347, 5.400000000000034994 ) ;
#7790=EDGE_LOOP ( 'NONE', ( #7224, #2381, #5945 ) ) ;
#7795=CARTESIAN_POINT ( 'NONE',  ( 1.110223024625156540E-13, 2.342598717236896722, -4.057500000000047180 ) ) ;
#7804=CYLINDRICAL_SURFACE ( 'NONE', #131, 5.000000000000034639 ) ;
#7810=EDGE_CURVE ( 'NONE', #4696, #6850, #5285, .T. ) ;
#7820=VERTEX_POINT ( 'NONE', #2674 ) ;
#7837=LINE ( 'NONE', #7884, #88 ) ;
#7851=AXIS2_PLACEMENT_3D ( 'NONE', #1774, #3083, #4432 ) ;
#7855=DIRECTION ( 'NONE',  ( -1.000000000000000000, 1.774937036747276562E-30, 0.000000000000000000 ) ) ;
#7858=FACE_BOUND ( 'NONE', #459, .T. ) ;
#7884=CARTESIAN_POINT ( 'NONE',  ( 5.000000000000004441, -2.342598717236951789, 4.057500000000047180 ) ) ;
#7893=VECTOR ( 'NONE', #6231, 1000.000000000000114 ) ;
#7895=ORIENTED_EDGE ( 'NONE', *, *, #529, .F. ) ;
#7937=CIRCLE ( 'NONE', #2115, 4.057500000000000107 ) ;
#7950=LINE ( 'NONE', #3332, #6040 ) ;
#7957=DIRECTION ( 'NONE',  ( 0.000000000000000000, -5.322451846059955323E-30, 1.000000000000000000 ) ) ;
#7975=AXIS2_PLACEMENT_3D ( 'NONE', #3970, #1405, #4759 ) ;
#7978=CARTESIAN_POINT ( 'NONE',  ( 0.000000000000000000, -2.342598717236902939, 4.057500000000047180 ) ) ;
#7983=ADVANCED_FACE ( 'NONE', ( #1452 ), #889, .F. ) ;
#7988=DIRECTION ( 'NONE',  ( -1.000000000000000000, 1.774937036747276562E-30, 0.000000000000000000 ) ) ;
#7991=AXIS2_PLACEMENT_3D ( 'NONE', #6779, #6820, #802 ) ;
#8002=LINE ( 'NONE', #4654, #7378 ) ;
#8018=EDGE_LOOP ( 'NONE', ( #6777, #2238, #1977, #333, #5021 ) ) ;
#8028=AXIS2_PLACEMENT_3D ( 'NONE', #346, #7013, #1554 ) ;
#8039=CARTESIAN_POINT ( 'NONE',  ( 0.000000000000000000, 0.000000000000000000, 0.000000000000000000 ) ) ;
#8055=VERTEX_POINT ( 'NONE', #5012 ) ;
#8069=CONICAL_SURFACE ( 'NONE', #5998, 4.171999999999999709, 0.7853981633975604115 ) ;
#8093=DIRECTION ( 'NONE',  ( 1.885870601543981347E-30, -1.000000000000000000, 7.405124331421681105E-16 ) ) ;
#8100=VERTEX_POINT ( 'NONE', #496 ) ;
#8101=CARTESIAN_POINT ( 'NONE',  ( 5.551115123125782702E-14, -2.342598717236909600, -4.057500000000047180 ) ) ;
#8104=EDGE_CURVE ( 'NONE', #4193, #367, #3331, .T. ) ;
#8106=VECTOR ( 'NONE', #2272, 1000.000000000000114 ) ;
#8113=ORIENTED_EDGE ( 'NONE', *, *, #222, .F. ) ;
#8122=FACE_OUTER_BOUND ( 'NONE', #5100, .T. ) ;
#8142=CARTESIAN_POINT ( 'NONE',  ( 5.000000000000004441, -2.342598717236951789, 4.057500000000047180 ) ) ;
#8147=CARTESIAN_POINT ( 'NONE',  ( 5.000000000000004441, 4.685197434473897360, 0.000000000000000000 ) ) ;
#8156=DIRECTION ( 'NONE',  ( 0.000000000000000000, 5.322451846059958826E-30, -1.000000000000000000 ) ) ;
#8157=ADVANCED_FACE ( 'NONE', ( #6619 ), #4131, .F. ) ;
#8167=CARTESIAN_POINT ( 'NONE',  ( 5.000000000000060396, -3.513898075855427461, -2.028750000000023590 ) ) ;
#8181=DIRECTION ( 'NONE',  ( 0.000000000000000000, 0.8660254037844394848, 0.4999999999999986122 ) ) ;
#8185=CARTESIAN_POINT ( 'NONE',  ( -31.74999999999994316, -1.972152263052529514E-28, 0.000000000000000000 ) ) ;
#8194=LINE ( 'NONE', #260, #1297 ) ;
#8197=CIRCLE ( 'NONE', #7207, 4.057500000000000107 ) ;
#8215=PLANE ( 'NONE',  #2498 ) ;
#8230=ORIENTED_EDGE ( 'NONE', *, *, #632, .F. ) ;
#8255=DIRECTION ( 'NONE',  ( -1.000000000000000000, 1.774937036747276562E-30, 0.000000000000000000 ) ) ;
#8267=CARTESIAN_POINT ( 'NONE',  ( 5.000000000000004441, -2.342598717236951789, 4.057500000000047180 ) ) ;
#8268=EDGE_CURVE ( 'NONE', #2641, #5555, #7350, .T. ) ;
#8294=ORIENTED_EDGE ( 'NONE', *, *, #5235, .T. ) ;
#8305=DIRECTION ( 'NONE',  ( 0.000000000000000000, 5.322451846059955323E-30, -1.000000000000000000 ) ) ;
#8306=AXIS2_PLACEMENT_3D ( 'NONE', #8039, #4028, #6011 ) ;
#8322=ADVANCED_FACE ( 'NONE', ( #2906 ), #7609, .F. ) ;
#8327=DIRECTION ( 'NONE',  ( -1.000000000000000000, 1.774937036747276562E-30, -0.000000000000000000 ) ) ;
#8334=DIRECTION ( 'NONE',  ( 0.7071067811865474617, 8.659560562354431192E-17, 0.7071067811865474617 ) ) ;
#8347=AXIS2_PLACEMENT_3D ( 'NONE', #5658, #1536, #4848 ) ;
#8356=ORIENTED_EDGE ( 'NONE', *, *, #4471, .F. ) ;
#8357=EDGE_CURVE ( 'NONE', #18, #4707, #3392, .T. ) ;
#8360=ORIENTED_EDGE ( 'NONE', *, *, #5738, .F. ) ;
#8366=DIRECTION ( 'NONE',  ( -1.000000000000000000, 1.774937036747276562E-30, 0.000000000000000000 ) ) ;
#8368=UNCERTAINTY_MEASURE_WITH_UNIT (LENGTH_MEASURE( 1.000000000000000082E-05 ), #4544, 'distance_accuracy_value', 'NONE');
#8381=FACE_OUTER_BOUND ( 'NONE', #7331, .T. ) ;
#8391=DIRECTION ( 'NONE',  ( -0.5000000000000042188, -3.721909990733644056E-30, 0.8660254037844361541 ) ) ;
#8419=LINE ( 'NONE', #6585, #3372 ) ;
#8489=VERTEX_POINT ( 'NONE', #593 ) ;
#8506=DIRECTION ( 'NONE',  ( 0.000000000000000000, 5.322451846059955323E-30, -1.000000000000000000 ) ) ;
#8526=ORIENTED_EDGE ( 'NONE', *, *, #2678, .T. ) ;
#8538=EDGE_CURVE ( 'NONE', #1999, #6850, #4089, .T. ) ;
#8551=DIRECTION ( 'NONE',  ( -1.000000000000000000, 1.774937036747276562E-30, 0.000000000000000000 ) ) ;
#8599=CARTESIAN_POINT ( 'NONE',  ( 10.40000000000001990, -4.129221776824974572E-28, 5.000000000000478728 ) ) ;
#8664=COLOUR_RGB('Black',0.12,0.14,0.17);
#8665=FILL_AREA_STYLE_COLOUR('',#8664);
#8666=FILL_AREA_STYLE('',(#8665));
#8667=SURFACE_STYLE_FILL_AREA(#8666);
#8668=SURFACE_SIDE_STYLE('',(#8667));
#8669=SURFACE_STYLE_USAGE(.BOTH.,#8668);
#8670=PRESENTATION_STYLE_ASSIGNMENT((#8669));
ENDSEC;
END-ISO-10303-21;
